ISO-10303-21;
HEADER;
/* Generated by software containing ST-Developer
 * from STEP Tools, Inc. (www.steptools.com) 
 */

FILE_DESCRIPTION(
/* description */ ('Pedal-braked fixed caster'),
/* implementation_level */ '2;1');

FILE_NAME(
/* name */ 'Flat Washer - M6.step',
/* time_stamp */ '2026-10-28T03:26:52-07:00',
/* author */ (''),
/* organization */ (''),
/* preprocessor_version */ 'ST-DEVELOPER v20.2',
/* originating_system */ 'Autodesk Translation Framework v15.17.0.0',
/* authorisation */ '');

FILE_SCHEMA (('AUTOMOTIVE_DESIGN { 1 0 10303 214 3 1 1 }'));
ENDSEC;

DATA;
#10=MECHANICAL_DESIGN_GEOMETRIC_PRESENTATION_REPRESENTATION('',(#211),#5734);
#177=SHAPE_REPRESENTATION_RELATIONSHIP('SRR','None',#5815,#194);
#194=ADVANCED_BREP_SHAPE_REPRESENTATION('',(#234),#5719);
#211=STYLED_ITEM('',(#5991),#234);
#234=MANIFOLD_SOLID_BREP('Body1',#2993);
#270=CYLINDRICAL_SURFACE('',#3318,0.32);
#271=CYLINDRICAL_SURFACE('',#3321,0.6);
#318=FACE_BOUND('',#753,.T.);
#319=FACE_BOUND('',#755,.T.);
#377=CIRCLE('',#3319,0.32);
#378=CIRCLE('',#3320,0.32);
#379=CIRCLE('',#3322,0.6);
#380=CIRCLE('',#3323,0.6);
#549=FACE_OUTER_BOUND('',#750,.T.);
#550=FACE_OUTER_BOUND('',#751,.T.);
#551=FACE_OUTER_BOUND('',#752,.T.);
#552=FACE_OUTER_BOUND('',#754,.T.);
#750=EDGE_LOOP('',(#2270,#2271,#2272,#2273));
#751=EDGE_LOOP('',(#2274,#2275,#2276,#2277));
#752=EDGE_LOOP('',(#2278));
#753=EDGE_LOOP('',(#2279));
#754=EDGE_LOOP('',(#2280));
#755=EDGE_LOOP('',(#2281));
#1005=LINE('',#4854,#1217);
#1006=LINE('',#4860,#1218);
#1217=VECTOR('',#3929,0.32);
#1218=VECTOR('',#3936,0.6);
#1410=VERTEX_POINT('',#4851);
#1411=VERTEX_POINT('',#4853);
#1412=VERTEX_POINT('',#4857);
#1413=VERTEX_POINT('',#4859);
#1725=EDGE_CURVE('',#1410,#1410,#377,.T.);
#1726=EDGE_CURVE('',#1410,#1411,#1005,.T.);
#1727=EDGE_CURVE('',#1411,#1411,#378,.T.);
#1728=EDGE_CURVE('',#1412,#1412,#379,.T.);
#1729=EDGE_CURVE('',#1412,#1413,#1006,.T.);
#1730=EDGE_CURVE('',#1413,#1413,#380,.T.);
#2270=ORIENTED_EDGE('',*,*,#1725,.F.);
#2271=ORIENTED_EDGE('',*,*,#1726,.T.);
#2272=ORIENTED_EDGE('',*,*,#1727,.T.);
#2273=ORIENTED_EDGE('',*,*,#1726,.F.);
#2274=ORIENTED_EDGE('',*,*,#1728,.F.);
#2275=ORIENTED_EDGE('',*,*,#1729,.T.);
#2276=ORIENTED_EDGE('',*,*,#1730,.T.);
#2277=ORIENTED_EDGE('',*,*,#1729,.F.);
#2278=ORIENTED_EDGE('',*,*,#1728,.T.);
#2279=ORIENTED_EDGE('',*,*,#1725,.T.);
#2280=ORIENTED_EDGE('',*,*,#1730,.F.);
#2281=ORIENTED_EDGE('',*,*,#1727,.F.);
#2753=PLANE('',#3324);
#2754=PLANE('',#3325);
#2882=ADVANCED_FACE('',(#549),#270,.F.);
#2883=ADVANCED_FACE('',(#550),#271,.T.);
#2884=ADVANCED_FACE('',(#551,#318),#2753,.T.);
#2885=ADVANCED_FACE('',(#552,#319),#2754,.F.);
#2993=CLOSED_SHELL('',(#2882,#2883,#2884,#2885));
#3317=AXIS2_PLACEMENT_3D('',#4849,#3923,#3924);
#3318=AXIS2_PLACEMENT_3D('',#4850,#3925,#3926);
#3319=AXIS2_PLACEMENT_3D('',#4852,#3927,#3928);
#3320=AXIS2_PLACEMENT_3D('',#4855,#3930,#3931);
#3321=AXIS2_PLACEMENT_3D('',#4856,#3932,#3933);
#3322=AXIS2_PLACEMENT_3D('',#4858,#3934,#3935);
#3323=AXIS2_PLACEMENT_3D('',#4861,#3937,#3938);
#3324=AXIS2_PLACEMENT_3D('',#4862,#3939,#3940);
#3325=AXIS2_PLACEMENT_3D('',#4863,#3941,#3942);
#3923=DIRECTION('axis',(0.,0.,1.));
#3924=DIRECTION('refdir',(1.,0.,0.));
#3925=DIRECTION('center_axis',(0.,1.,0.));
#3926=DIRECTION('ref_axis',(1.,0.,0.));
#3927=DIRECTION('center_axis',(0.,-1.,0.));
#3928=DIRECTION('ref_axis',(1.,0.,0.));
#3929=DIRECTION('',(0.,-1.,0.));
#3930=DIRECTION('center_axis',(0.,-1.,0.));
#3931=DIRECTION('ref_axis',(1.,0.,0.));
#3932=DIRECTION('center_axis',(0.,1.,0.));
#3933=DIRECTION('ref_axis',(1.,0.,0.));
#3934=DIRECTION('center_axis',(0.,1.,0.));
#3935=DIRECTION('ref_axis',(1.,0.,0.));
#3936=DIRECTION('',(0.,-1.,0.));
#3937=DIRECTION('center_axis',(0.,1.,0.));
#3938=DIRECTION('ref_axis',(1.,0.,0.));
#3939=DIRECTION('center_axis',(0.,1.,0.));
#3940=DIRECTION('ref_axis',(1.,0.,0.));
#3941=DIRECTION('center_axis',(0.,1.,0.));
#3942=DIRECTION('ref_axis',(1.,0.,0.));
#4849=CARTESIAN_POINT('',(0.,0.,0.));
#4850=CARTESIAN_POINT('Origin',(0.,0.,0.));
#4851=CARTESIAN_POINT('',(-0.32,0.16,3.91886975727153E-17));
#4852=CARTESIAN_POINT('Origin',(0.,0.16,0.));
#4853=CARTESIAN_POINT('',(-0.32,0.,3.91886975727153E-17));
#4854=CARTESIAN_POINT('',(-0.32,0.,3.91886975727153E-17));
#4855=CARTESIAN_POINT('Origin',(0.,0.,0.));
#4856=CARTESIAN_POINT('Origin',(0.,0.,0.));
#4857=CARTESIAN_POINT('',(-0.6,0.16,7.34788079488412E-17));
#4858=CARTESIAN_POINT('Origin',(0.,0.16,0.));
#4859=CARTESIAN_POINT('',(-0.6,0.,7.34788079488412E-17));
#4860=CARTESIAN_POINT('',(-0.6,0.,7.34788079488412E-17));
#4861=CARTESIAN_POINT('Origin',(0.,0.,0.));
#4862=CARTESIAN_POINT('Origin',(0.,0.16,0.));
#4863=CARTESIAN_POINT('Origin',(0.,0.,0.));
#5696=UNCERTAINTY_MEASURE_WITH_UNIT(LENGTH_MEASURE(0.001),#5735,
'DISTANCE_ACCURACY_VALUE',
'Maximum model space distance between geometric entities at asserted c
onnectivities');
#5711=UNCERTAINTY_MEASURE_WITH_UNIT(LENGTH_MEASURE(0.001),#5735,
'DISTANCE_ACCURACY_VALUE',
'Maximum model space distance between geometric entities at asserted c
onnectivities');
#5719=(
GEOMETRIC_REPRESENTATION_CONTEXT(3)
GLOBAL_UNCERTAINTY_ASSIGNED_CONTEXT((#5696))
GLOBAL_UNIT_ASSIGNED_CONTEXT((#5735,#5737,#5738))
REPRESENTATION_CONTEXT('','3D')
);
#5734=(
GEOMETRIC_REPRESENTATION_CONTEXT(3)
GLOBAL_UNCERTAINTY_ASSIGNED_CONTEXT((#5711))
GLOBAL_UNIT_ASSIGNED_CONTEXT((#5735,#5737,#5738))
REPRESENTATION_CONTEXT('','3D')
);
#5735=(
LENGTH_UNIT()
NAMED_UNIT(*)
SI_UNIT(.CENTI.,.METRE.)
);
#5737=(
NAMED_UNIT(*)
PLANE_ANGLE_UNIT()
SI_UNIT($,.RADIAN.)
);
#5738=(
NAMED_UNIT(*)
SI_UNIT($,.STERADIAN.)
SOLID_ANGLE_UNIT()
);
#5746=SHAPE_DEFINITION_REPRESENTATION(#5768,#5815);
#5768=PRODUCT_DEFINITION_SHAPE('',$,#5838);
#5815=SHAPE_REPRESENTATION('',(#3317),#5719);
#5830=PRODUCT_DEFINITION_CONTEXT('part definition',#5898,'design');
#5838=PRODUCT_DEFINITION('Flat Washer - M6','Flat Washer - M6',#5860,#5830);
#5860=PRODUCT_DEFINITION_FORMATION('',$,#5907);
#5898=APPLICATION_CONTEXT(
'Core Data for Automotive Mechanical Design Process');
#5899=PRODUCT_CONTEXT('part definition',#5898,'mechanical');
#5907=PRODUCT('Flat Washer - M6','Flat Washer - M6','Flat Washer - M6',
(#5899));
#5985=COLOUR_RGB('Black',0.12,0.14,0.17);
#5986=FILL_AREA_STYLE_COLOUR('',#5985);
#5987=FILL_AREA_STYLE('',(#5986));
#5988=SURFACE_STYLE_FILL_AREA(#5987);
#5989=SURFACE_SIDE_STYLE('',(#5988));
#5990=SURFACE_STYLE_USAGE(.BOTH.,#5989);
#5991=PRESENTATION_STYLE_ASSIGNMENT((#5990));
ENDSEC;
END-ISO-10303-21;
